ISO-10303-21;
HEADER;
/* Generated by software containing ST-Developer
 * from STEP Tools, Inc. (www.steptools.com) 
 */
/* OPTION: using custom renumber hook */

FILE_DESCRIPTION(
/* description */ ('STEP AP242 Edition 2', 'CAx-IF Rec.Pracs.---Representation and Presentation of Product Manufa
cturing Information (PMI)---4.0---2014-10-13', 'CAx-IF Rec.Pracs.---3D Tessellated Geometry---0.4---2014-09-14', '2;1', 'CAx-IF Rec.Pracs.---User Defined Attributes---1.5---2016-08-15'),
/* implementation_level */ '2;1');

FILE_NAME(
/* name */ 'Slotted cheese head screw M2.5x0.45 x 6.step',
/* time_stamp */ '2026-10-09T13:59:33Z',
/* author */ (''),
/* organization */ (''),
/* preprocessor_version */ 'ST-DEVELOPER v20',
/* originating_system */ 'ONSHAPE BY PTC INC, 1.221',
/* authorisation */ '  ');

FILE_SCHEMA (('AP242_MANAGED_MODEL_BASED_3D_ENGINEERING_MIM_LF { 1 0 10303 442 3 1 4 }'));
ENDSEC;

DATA;
#15=CONICAL_SURFACE('',#6491,0.00209252040565334,0.0872664625997158);
#16=CONICAL_SURFACE('',#6503,0.00100643035625,0.785398163397448);
#32=TOROIDAL_SURFACE('',#6482,0.0020008872882516,0.0001);
#33=TOROIDAL_SURFACE('',#6498,0.00135,0.0001);
#34=TOROIDAL_SURFACE('',#6499,0.0020008872882516,0.0001);
#315=LINE('',#10064,#599);
#316=LINE('',#10092,#600);
#317=LINE('',#10135,#601);
#318=LINE('',#10136,#602);
#599=VECTOR('',#8339,1.);
#600=VECTOR('',#8360,1.);
#601=VECTOR('',#8381,1.);
#602=VECTOR('',#8382,1.);
#684=SHAPE_REPRESENTATION_RELATIONSHIP('','',#5703,#698);
#698=ADVANCED_BREP_SHAPE_REPRESENTATION('',(#5671),#10157);
#783=PLANE('',#6480);
#784=PLANE('',#6488);
#785=PLANE('',#6490);
#786=PLANE('',#6496);
#787=PLANE('',#6500);
#788=PLANE('',#6501);
#789=PLANE('',#6502);
#806=B_SPLINE_CURVE_WITH_KNOTS('',3,(#10072,#10073,#10074,#10075),
 .UNSPECIFIED.,.F.,.F.,(4,4),(0.000582701576065907,0.000731093758582388),
 .UNSPECIFIED.);
#807=B_SPLINE_CURVE_WITH_KNOTS('',3,(#10079,#10080,#10081,#10082),
 .UNSPECIFIED.,.F.,.F.,(4,4),(0.000110312006623771,0.000258881093106313),
 .UNSPECIFIED.);
#808=B_SPLINE_CURVE_WITH_KNOTS('',3,(#10097,#10098,#10099,#10100),
 .UNSPECIFIED.,.F.,.F.,(4,4),(0.00363875425759936,0.00424984212477264),
 .UNSPECIFIED.);
#809=B_SPLINE_CURVE_WITH_KNOTS('',3,(#10104,#10105,#10106,#10107),
 .UNSPECIFIED.,.F.,.F.,(4,4),(0.00363875425759936,0.00424984212477264),
 .UNSPECIFIED.);
#810=B_SPLINE_CURVE_WITH_KNOTS('',3,(#10108,#10109,#10110,#10111),
 .UNSPECIFIED.,.F.,.F.,(4,4),(0.00356470722087229,0.00417579509082418),
 .UNSPECIFIED.);
#811=B_SPLINE_CURVE_WITH_KNOTS('',3,(#10115,#10116,#10117,#10118),
 .UNSPECIFIED.,.F.,.F.,(4,4),(0.00356470722087229,0.00417579509082374),
 .UNSPECIFIED.);
#812=B_SPLINE_CURVE_WITH_KNOTS('',3,(#10126,#10127,#10128,#10129),
 .UNSPECIFIED.,.F.,.F.,(4,4),(0.000582701576065907,0.000731093758582387),
 .UNSPECIFIED.);
#813=B_SPLINE_CURVE_WITH_KNOTS('',3,(#10130,#10131,#10132,#10133),
 .UNSPECIFIED.,.F.,.F.,(4,4),(0.000110312006623771,0.000258881093106891),
 .UNSPECIFIED.);
#2298=ORIENTED_EDGE('',*,*,#3086,.F.);
#2299=ORIENTED_EDGE('',*,*,#3087,.T.);
#2300=ORIENTED_EDGE('',*,*,#3088,.F.);
#2301=ORIENTED_EDGE('',*,*,#3089,.T.);
#2302=ORIENTED_EDGE('',*,*,#3090,.F.);
#2303=ORIENTED_EDGE('',*,*,#3091,.T.);
#2304=ORIENTED_EDGE('',*,*,#3092,.T.);
#2305=ORIENTED_EDGE('',*,*,#3093,.T.);
#2306=ORIENTED_EDGE('',*,*,#3094,.T.);
#2307=ORIENTED_EDGE('',*,*,#3090,.T.);
#2308=ORIENTED_EDGE('',*,*,#3095,.T.);
#2309=ORIENTED_EDGE('',*,*,#3096,.T.);
#2310=ORIENTED_EDGE('',*,*,#3097,.T.);
#2311=ORIENTED_EDGE('',*,*,#3098,.F.);
#2312=ORIENTED_EDGE('',*,*,#3099,.F.);
#2313=ORIENTED_EDGE('',*,*,#3088,.T.);
#2314=ORIENTED_EDGE('',*,*,#3100,.F.);
#2315=ORIENTED_EDGE('',*,*,#3101,.F.);
#2316=ORIENTED_EDGE('',*,*,#3102,.T.);
#2317=ORIENTED_EDGE('',*,*,#3103,.F.);
#2318=ORIENTED_EDGE('',*,*,#3104,.F.);
#2319=ORIENTED_EDGE('',*,*,#3103,.T.);
#2320=ORIENTED_EDGE('',*,*,#3104,.T.);
#2321=ORIENTED_EDGE('',*,*,#3093,.F.);
#2322=ORIENTED_EDGE('',*,*,#3105,.F.);
#2323=ORIENTED_EDGE('',*,*,#3096,.F.);
#2324=ORIENTED_EDGE('',*,*,#3106,.F.);
#2325=ORIENTED_EDGE('',*,*,#3087,.F.);
#2326=ORIENTED_EDGE('',*,*,#3098,.T.);
#2327=ORIENTED_EDGE('',*,*,#3107,.T.);
#2328=ORIENTED_EDGE('',*,*,#3101,.T.);
#2329=ORIENTED_EDGE('',*,*,#3108,.F.);
#2330=ORIENTED_EDGE('',*,*,#3105,.T.);
#2331=ORIENTED_EDGE('',*,*,#3086,.T.);
#2332=ORIENTED_EDGE('',*,*,#3106,.T.);
#2333=ORIENTED_EDGE('',*,*,#3102,.F.);
#2334=ORIENTED_EDGE('',*,*,#3107,.F.);
#2335=ORIENTED_EDGE('',*,*,#3097,.F.);
#2336=ORIENTED_EDGE('',*,*,#3099,.T.);
#2337=ORIENTED_EDGE('',*,*,#3108,.T.);
#2338=ORIENTED_EDGE('',*,*,#3100,.T.);
#2339=ORIENTED_EDGE('',*,*,#3091,.F.);
#2340=ORIENTED_EDGE('',*,*,#3095,.F.);
#2341=ORIENTED_EDGE('',*,*,#3089,.F.);
#2342=ORIENTED_EDGE('',*,*,#3092,.F.);
#2343=ORIENTED_EDGE('',*,*,#3094,.F.);
#3086=EDGE_CURVE('',#3633,#3634,#315,.T.);
#3087=EDGE_CURVE('',#3633,#3634,#4096,.F.);
#3088=EDGE_CURVE('',#3635,#3636,#4097,.F.);
#3089=EDGE_CURVE('',#3635,#3637,#806,.T.);
#3090=EDGE_CURVE('',#3638,#3637,#4098,.F.);
#3091=EDGE_CURVE('',#3638,#3636,#807,.T.);
#3092=EDGE_CURVE('',#3639,#3639,#4099,.T.);
#3093=EDGE_CURVE('',#3640,#3640,#4100,.T.);
#3094=EDGE_CURVE('',#3641,#3641,#4101,.F.);
#3095=EDGE_CURVE('',#3637,#3638,#316,.T.);
#3096=EDGE_CURVE('',#3642,#3643,#4102,.F.);
#3097=EDGE_CURVE('',#3643,#3644,#808,.T.);
#3098=EDGE_CURVE('',#3645,#3644,#4103,.T.);
#3099=EDGE_CURVE('',#3635,#3645,#809,.T.);
#3100=EDGE_CURVE('',#3646,#3636,#810,.T.);
#3101=EDGE_CURVE('',#3647,#3646,#4104,.T.);
#3102=EDGE_CURVE('',#3647,#3642,#811,.T.);
#3103=EDGE_CURVE('',#3648,#3648,#4105,.T.);
#3104=EDGE_CURVE('',#3649,#3649,#4106,.T.);
#3105=EDGE_CURVE('',#3643,#3633,#812,.T.);
#3106=EDGE_CURVE('',#3634,#3642,#813,.T.);
#3107=EDGE_CURVE('',#3644,#3647,#317,.T.);
#3108=EDGE_CURVE('',#3645,#3646,#318,.T.);
#3633=VERTEX_POINT('',#10065);
#3634=VERTEX_POINT('',#10066);
#3635=VERTEX_POINT('',#10070);
#3636=VERTEX_POINT('',#10071);
#3637=VERTEX_POINT('',#10076);
#3638=VERTEX_POINT('',#10078);
#3639=VERTEX_POINT('',#10085);
#3640=VERTEX_POINT('',#10087);
#3641=VERTEX_POINT('',#10090);
#3642=VERTEX_POINT('',#10095);
#3643=VERTEX_POINT('',#10096);
#3644=VERTEX_POINT('',#10101);
#3645=VERTEX_POINT('',#10103);
#3646=VERTEX_POINT('',#10112);
#3647=VERTEX_POINT('',#10114);
#3648=VERTEX_POINT('',#10120);
#3649=VERTEX_POINT('',#10123);
#4096=CIRCLE('',#6481,0.0020008872882516);
#4097=CIRCLE('',#6483,0.00210050675806077);
#4098=CIRCLE('',#6484,0.0020008872882516);
#4099=CIRCLE('',#6486,0.00125);
#4100=CIRCLE('',#6487,0.00125);
#4101=CIRCLE('',#6489,0.00100643035625);
#4102=CIRCLE('',#6492,0.00210050675806077);
#4103=CIRCLE('',#6493,0.00215376247012148);
#4104=CIRCLE('',#6494,0.00215376247012148);
#4105=CIRCLE('',#6495,0.00225);
#4106=CIRCLE('',#6497,0.00135);
#4537=EDGE_LOOP('',(#2298,#2299));
#4538=EDGE_LOOP('',(#2300,#2301,#2302,#2303));
#4539=EDGE_LOOP('',(#2304));
#4540=EDGE_LOOP('',(#2305));
#4541=EDGE_LOOP('',(#2306));
#4542=EDGE_LOOP('',(#2307,#2308));
#4543=EDGE_LOOP('',(#2309,#2310,#2311,#2312,#2313,#2314,#2315,#2316));
#4544=EDGE_LOOP('',(#2317));
#4545=EDGE_LOOP('',(#2318));
#4546=EDGE_LOOP('',(#2319));
#4547=EDGE_LOOP('',(#2320));
#4548=EDGE_LOOP('',(#2321));
#4549=EDGE_LOOP('',(#2322,#2323,#2324,#2325));
#4550=EDGE_LOOP('',(#2326,#2327,#2328,#2329));
#4551=EDGE_LOOP('',(#2330,#2331,#2332,#2333,#2334,#2335));
#4552=EDGE_LOOP('',(#2336,#2337,#2338,#2339,#2340,#2341));
#4553=EDGE_LOOP('',(#2342));
#4554=EDGE_LOOP('',(#2343));
#4985=FACE_BOUND('',#4537,.T.);
#4986=FACE_BOUND('',#4538,.T.);
#4987=FACE_BOUND('',#4539,.T.);
#4988=FACE_BOUND('',#4540,.T.);
#4989=FACE_BOUND('',#4541,.T.);
#4990=FACE_BOUND('',#4542,.T.);
#4991=FACE_BOUND('',#4543,.T.);
#4992=FACE_BOUND('',#4544,.T.);
#4993=FACE_BOUND('',#4545,.T.);
#4994=FACE_BOUND('',#4546,.T.);
#4995=FACE_BOUND('',#4547,.T.);
#4996=FACE_BOUND('',#4548,.T.);
#4997=FACE_BOUND('',#4549,.T.);
#4998=FACE_BOUND('',#4550,.T.);
#4999=FACE_BOUND('',#4551,.T.);
#5000=FACE_BOUND('',#4552,.T.);
#5001=FACE_BOUND('',#4553,.T.);
#5002=FACE_BOUND('',#4554,.T.);
#5212=CYLINDRICAL_SURFACE('',#6485,0.00125);
#5526=ADVANCED_FACE('',(#4985),#783,.F.);
#5527=ADVANCED_FACE('',(#4986),#32,.T.);
#5528=ADVANCED_FACE('',(#4987,#4988),#5212,.T.);
#5529=ADVANCED_FACE('',(#4989),#784,.F.);
#5530=ADVANCED_FACE('',(#4990),#785,.F.);
#5531=ADVANCED_FACE('',(#4991,#4992),#15,.T.);
#5532=ADVANCED_FACE('',(#4993,#4994),#786,.F.);
#5533=ADVANCED_FACE('',(#4995,#4996),#33,.F.);
#5534=ADVANCED_FACE('',(#4997),#34,.T.);
#5535=ADVANCED_FACE('',(#4998),#787,.T.);
#5536=ADVANCED_FACE('',(#4999),#788,.F.);
#5537=ADVANCED_FACE('',(#5000),#789,.T.);
#5538=ADVANCED_FACE('',(#5001,#5002),#16,.T.);
#5552=CLOSED_SHELL('',(#5526,#5527,#5528,#5529,#5530,#5531,#5532,#5533,
#5534,#5535,#5536,#5537,#5538));
#5566=STYLED_ITEM('',(#5580),#5671);
#5580=PRESENTATION_STYLE_ASSIGNMENT((#5594));
#5594=SURFACE_STYLE_USAGE(.BOTH.,#5608);
#5608=SURFACE_SIDE_STYLE('',(#5622));
#5622=SURFACE_STYLE_FILL_AREA(#5636);
#5636=FILL_AREA_STYLE('',(#5650));
#5650=FILL_AREA_STYLE_COLOUR('',#5652);
#5652=COLOUR_RGB('', 0.31764706, 0.68627451, 0.89019608);
#5671=MANIFOLD_SOLID_BREP('Slotted cheese head screw M2.5x0.45 x 6',#5552);
#5687=SHAPE_DEFINITION_REPRESENTATION(#10208,#5703);
#5703=SHAPE_REPRESENTATION('Slotted cheese head screw M2.5x0.45 x 6',(#5704),
#10157);
#5704=AXIS2_PLACEMENT_3D('',#8391,#6505,#6506);
#6480=AXIS2_PLACEMENT_3D('',#10063,#8337,#8338);
#6481=AXIS2_PLACEMENT_3D('',#10067,#8340,#8341);
#6482=AXIS2_PLACEMENT_3D('',#10068,#8342,#8343);
#6483=AXIS2_PLACEMENT_3D('',#10069,#8344,#8345);
#6484=AXIS2_PLACEMENT_3D('',#10077,#8346,#8347);
#6485=AXIS2_PLACEMENT_3D('',#10083,#8348,#8349);
#6486=AXIS2_PLACEMENT_3D('',#10084,#8350,#8351);
#6487=AXIS2_PLACEMENT_3D('',#10086,#8352,#8353);
#6488=AXIS2_PLACEMENT_3D('',#10088,#8354,#8355);
#6489=AXIS2_PLACEMENT_3D('',#10089,#8356,#8357);
#6490=AXIS2_PLACEMENT_3D('',#10091,#8358,#8359);
#6491=AXIS2_PLACEMENT_3D('',#10093,#8361,#8362);
#6492=AXIS2_PLACEMENT_3D('',#10094,#8363,#8364);
#6493=AXIS2_PLACEMENT_3D('',#10102,#8365,#8366);
#6494=AXIS2_PLACEMENT_3D('',#10113,#8367,#8368);
#6495=AXIS2_PLACEMENT_3D('',#10119,#8369,#8370);
#6496=AXIS2_PLACEMENT_3D('',#10121,#8371,#8372);
#6497=AXIS2_PLACEMENT_3D('',#10122,#8373,#8374);
#6498=AXIS2_PLACEMENT_3D('',#10124,#8375,#8376);
#6499=AXIS2_PLACEMENT_3D('',#10125,#8377,#8378);
#6500=AXIS2_PLACEMENT_3D('',#10134,#8379,#8380);
#6501=AXIS2_PLACEMENT_3D('',#10137,#8383,#8384);
#6502=AXIS2_PLACEMENT_3D('',#10138,#8385,#8386);
#6503=AXIS2_PLACEMENT_3D('',#10139,#8387,#8388);
#6505=DIRECTION('',(0.,0.,1.));
#6506=DIRECTION('',(1.,0.,0.));
#8337=DIRECTION('',(0.,0.,-1.));
#8338=DIRECTION('',(-1.,0.,0.));
#8339=DIRECTION('',(1.,0.,0.));
#8340=DIRECTION('',(0.,0.,-1.));
#8341=DIRECTION('',(-1.,0.,0.));
#8342=DIRECTION('',(0.,0.,-1.));
#8343=DIRECTION('',(-1.,0.,0.));
#8344=DIRECTION('',(0.,0.,1.));
#8345=DIRECTION('',(1.,0.,0.));
#8346=DIRECTION('',(0.,0.,-1.));
#8347=DIRECTION('',(-1.,0.,0.));
#8348=DIRECTION('',(0.,0.,-1.));
#8349=DIRECTION('',(-1.,0.,0.));
#8350=DIRECTION('',(0.,0.,1.));
#8351=DIRECTION('',(1.,0.,0.));
#8352=DIRECTION('',(0.,0.,-1.));
#8353=DIRECTION('',(-1.,0.,0.));
#8354=DIRECTION('',(0.,0.,1.));
#8355=DIRECTION('',(1.,0.,0.));
#8356=DIRECTION('',(0.,0.,1.));
#8357=DIRECTION('',(1.,0.,0.));
#8358=DIRECTION('',(0.,0.,-1.));
#8359=DIRECTION('',(-1.,0.,0.));
#8360=DIRECTION('',(1.,0.,0.));
#8361=DIRECTION('',(0.,0.,-1.));
#8362=DIRECTION('',(-1.,0.,0.));
#8363=DIRECTION('',(0.,0.,1.));
#8364=DIRECTION('',(1.,0.,0.));
#8365=DIRECTION('',(0.,0.,1.));
#8366=DIRECTION('',(1.,0.,0.));
#8367=DIRECTION('',(0.,0.,1.));
#8368=DIRECTION('',(1.,0.,0.));
#8369=DIRECTION('',(0.,0.,-1.));
#8370=DIRECTION('',(-1.,0.,0.));
#8371=DIRECTION('',(0.,0.,1.));
#8372=DIRECTION('',(1.,0.,0.));
#8373=DIRECTION('',(0.,0.,-1.));
#8374=DIRECTION('',(-1.,0.,0.));
#8375=DIRECTION('',(0.,0.,-1.));
#8376=DIRECTION('',(-1.,0.,0.));
#8377=DIRECTION('',(0.,0.,-1.));
#8378=DIRECTION('',(-1.,0.,0.));
#8379=DIRECTION('',(0.,0.,1.));
#8380=DIRECTION('',(1.,0.,0.));
#8381=DIRECTION('',(1.,0.,0.));
#8382=DIRECTION('',(1.,0.,0.));
#8383=DIRECTION('',(0.,-1.,0.));
#8384=DIRECTION('',(0.,0.,-1.));
#8385=DIRECTION('',(0.,-1.,0.));
#8386=DIRECTION('',(0.,0.,-1.));
#8387=DIRECTION('',(0.,0.,1.));
#8388=DIRECTION('',(1.,0.,0.));
#8391=CARTESIAN_POINT('',(0.,0.,0.));
#10063=CARTESIAN_POINT('',(-0.00104626020282667,0.,6.50521303491303E-19));
#10064=CARTESIAN_POINT('',(0.,-0.0003,6.50521303491303E-19));
#10065=CARTESIAN_POINT('',(-0.00197826943066075,-0.0003,6.50521303491303E-19));
#10066=CARTESIAN_POINT('',(0.00197826943066075,-0.0003,6.50521303491303E-19));
#10067=CARTESIAN_POINT('',(0.,0.,6.50521303491303E-19));
#10068=CARTESIAN_POINT('',(0.,0.,-0.0001));
#10069=CARTESIAN_POINT('',(0.,0.,-9.12844257252368E-5));
#10070=CARTESIAN_POINT('',(-0.00207897297737586,0.0003,-9.12844257252367E-5));
#10071=CARTESIAN_POINT('',(0.00207897297737584,0.0003,-9.12844257252368E-5));
#10072=CARTESIAN_POINT('',(-0.00207897297737584,0.0003,-9.12844257252392E-5));
#10073=CARTESIAN_POINT('',(-0.00207459712624839,0.0003,-4.17809699915527E-5));
#10074=CARTESIAN_POINT('',(-0.00202837661239549,0.0003,-6.48859435981983E-19));
#10075=CARTESIAN_POINT('',(-0.00197826943066076,0.0003,3.05634754505891E-21));
#10076=CARTESIAN_POINT('',(-0.00197826943066075,0.0003,6.50521303491303E-19));
#10077=CARTESIAN_POINT('',(0.,0.,6.50521303491303E-19));
#10078=CARTESIAN_POINT('',(0.00197826943066075,0.0003,6.50521303491303E-19));
#10079=CARTESIAN_POINT('',(0.00197826943066076,0.0003,1.75840007344507E-18));
#10080=CARTESIAN_POINT('',(0.00202795255984864,0.0003,1.11200139422846E-18));
#10081=CARTESIAN_POINT('',(0.00207460838288334,0.0003,-4.19083148928644E-5));
#10082=CARTESIAN_POINT('',(0.00207897297737584,0.0003,-9.12844257252363E-5));
#10083=CARTESIAN_POINT('',(0.,0.,-0.0039));
#10084=CARTESIAN_POINT('',(0.,0.,-0.00755643035625));
#10085=CARTESIAN_POINT('',(0.00125,0.,-0.00755643035625));
#10086=CARTESIAN_POINT('',(0.,0.,-0.0019));
#10087=CARTESIAN_POINT('',(-0.00125,0.,-0.0019));
#10088=CARTESIAN_POINT('',(-0.000625,0.,-0.0078));
#10089=CARTESIAN_POINT('',(0.,0.,-0.0078));
#10090=CARTESIAN_POINT('',(0.00100643035625,0.,-0.0078));
#10091=CARTESIAN_POINT('',(-0.00104626020282667,0.,6.50521303491303E-19));
#10092=CARTESIAN_POINT('',(-5.01008275896316E-5,0.0003,6.50521303491303E-19));
#10093=CARTESIAN_POINT('',(0.,0.,1.3010426069826E-18));
#10094=CARTESIAN_POINT('',(0.,0.,-9.12844257252368E-5));
#10095=CARTESIAN_POINT('',(0.00207897297737919,-0.0003,-9.12844257253807E-5));
#10096=CARTESIAN_POINT('',(-0.00207897297737586,-0.0003,-9.12844257252367E-5));
#10097=CARTESIAN_POINT('',(-0.00207897297737588,-0.0003,-9.12844257252349E-5));
#10098=CARTESIAN_POINT('',(-0.00209690871796292,-0.0003,-0.000294189212551694));
#10099=CARTESIAN_POINT('',(-0.00211483976375729,-0.0003,-0.000497094414503252));
#10100=CARTESIAN_POINT('',(-0.00213276646112605,-0.0003,-0.000699999999999994));
#10101=CARTESIAN_POINT('',(-0.00213276646112597,-0.0003,-0.0007));
#10102=CARTESIAN_POINT('',(0.,0.,-0.0007));
#10103=CARTESIAN_POINT('',(-0.00213276646112597,0.0003,-0.0007));
#10104=CARTESIAN_POINT('',(-0.00207897297737588,0.0003,-9.12844257252349E-5));
#10105=CARTESIAN_POINT('',(-0.00209690871796292,0.0003,-0.000294189212551693));
#10106=CARTESIAN_POINT('',(-0.00211483976375729,0.0003,-0.000497094414503251));
#10107=CARTESIAN_POINT('',(-0.00213276646112605,0.0003,-0.000699999999999993));
#10108=CARTESIAN_POINT('',(0.00213276646112605,0.0003,-0.000699999999999993));
#10109=CARTESIAN_POINT('',(0.00211483976374572,0.0003,-0.000497094414372398));
#10110=CARTESIAN_POINT('',(0.00209690871792154,0.0003,-0.000294189212083583));
#10111=CARTESIAN_POINT('',(0.00207897297737588,0.0003,-9.12844257252331E-5));
#10112=CARTESIAN_POINT('',(0.00213276646112597,0.0003,-0.0007));
#10113=CARTESIAN_POINT('',(0.,0.,-0.0007));
#10114=CARTESIAN_POINT('',(0.00213276646112597,-0.0003,-0.0007));
#10115=CARTESIAN_POINT('',(0.00213276646112605,-0.0003,-0.000699999999999993));
#10116=CARTESIAN_POINT('',(0.00211483976374574,-0.0003,-0.000497094414372544));
#10117=CARTESIAN_POINT('',(0.00209690871792157,-0.0003,-0.000294189212083876));
#10118=CARTESIAN_POINT('',(0.00207897297737592,-0.0003,-9.12844257256711E-5));
#10119=CARTESIAN_POINT('',(0.,0.,-0.0018));
#10120=CARTESIAN_POINT('',(-0.00225,0.,-0.0018));
#10121=CARTESIAN_POINT('',(-0.0018,0.,-0.0018));
#10122=CARTESIAN_POINT('',(0.,0.,-0.0018));
#10123=CARTESIAN_POINT('',(-0.00135,0.,-0.0018));
#10124=CARTESIAN_POINT('',(0.,0.,-0.0019));
#10125=CARTESIAN_POINT('',(0.,0.,-0.0001));
#10126=CARTESIAN_POINT('',(-0.00207897297737584,-0.0003,-9.12844257252392E-5));
#10127=CARTESIAN_POINT('',(-0.00207459712624839,-0.0003,-4.17809699915526E-5));
#10128=CARTESIAN_POINT('',(-0.00202837661239549,-0.0003,-6.54219152761022E-19));
#10129=CARTESIAN_POINT('',(-0.00197826943066076,-0.0003,-2.30336923397844E-21));
#10130=CARTESIAN_POINT('',(0.00197826943066075,-0.0003,1.76771743586486E-18));
#10131=CARTESIAN_POINT('',(0.00202795255984883,-0.0003,1.12131875664574E-18));
#10132=CARTESIAN_POINT('',(0.00207460838288366,-0.0003,-4.19083148932107E-5));
#10133=CARTESIAN_POINT('',(0.00207897297737589,-0.0003,-9.12844257258122E-5));
#10134=CARTESIAN_POINT('',(0.,0.,-0.0007));
#10135=CARTESIAN_POINT('',(0.,-0.0003,-0.0007));
#10136=CARTESIAN_POINT('',(-5.01008275896316E-5,0.0003,-0.0007));
#10137=CARTESIAN_POINT('',(0.,-0.0003,-0.0007));
#10138=CARTESIAN_POINT('',(-5.01008275896316E-5,0.0003,-0.0007));
#10139=CARTESIAN_POINT('',(0.,0.,-0.0078));
#10141=MECHANICAL_DESIGN_GEOMETRIC_PRESENTATION_REPRESENTATION('',(#5566),#10142);
#10142=(
GEOMETRIC_REPRESENTATION_CONTEXT(3)
GLOBAL_UNCERTAINTY_ASSIGNED_CONTEXT((#10158))
GLOBAL_UNIT_ASSIGNED_CONTEXT((#10176,#10175,#10174))
REPRESENTATION_CONTEXT('MAS-674','TOP_LEVEL_ASSEMBLY_PART')
);
#10157=(
GEOMETRIC_REPRESENTATION_CONTEXT(3)
GLOBAL_UNCERTAINTY_ASSIGNED_CONTEXT((#10173))
GLOBAL_UNIT_ASSIGNED_CONTEXT((#10176,#10175,#10174))
REPRESENTATION_CONTEXT('Slotted cheese head screw M2.5x0.45 x 6',
'COMPONENT_PART')
);
#10158=UNCERTAINTY_MEASURE_WITH_UNIT(LENGTH_MEASURE(1.E-8),#10176,
'DISTANCE_ACCURACY_VALUE','Maximum Tolerance applied to model');
#10173=UNCERTAINTY_MEASURE_WITH_UNIT(LENGTH_MEASURE(2.E-5),#10176,
'DISTANCE_ACCURACY_VALUE','Maximum Tolerance applied to model');
#10174=(
NAMED_UNIT(*)
SI_UNIT($,.STERADIAN.)
SOLID_ANGLE_UNIT()
);
#10175=(
NAMED_UNIT(*)
PLANE_ANGLE_UNIT()
SI_UNIT($,.RADIAN.)
);
#10176=(
LENGTH_UNIT()
NAMED_UNIT(*)
SI_UNIT($,.METRE.)
);
#10208=PRODUCT_DEFINITION_SHAPE('','',#10225);
#10225=PRODUCT_DEFINITION('','',#10257,#10241);
#10241=PRODUCT_DEFINITION_CONTEXT('',#10323,'design');
#10257=PRODUCT_DEFINITION_FORMATION_WITH_SPECIFIED_SOURCE('','',#10289,
 .NOT_KNOWN.);
#10289=PRODUCT('Slotted cheese head screw M2.5x0.45 x 6',
'Slotted cheese head screw M2.5x0.45 x 6',
'Slotted cheese head screw M2.5x0.45 x 6',(#10321));
#10321=PRODUCT_CONTEXT('',#10323,'mechanical');
#10323=APPLICATION_CONTEXT('managed model based 3d engineering');
ENDSEC;
END-ISO-10303-21;
